ISO-10303-21;
HEADER;
FILE_DESCRIPTION (('STEP AP214'),
    '1' );
FILE_NAME ('Conveyor Speed Sensor Mount.step',
    '2026-10-28T18:30:06',
    ( '' ),
    ( '' ),
    'SwSTEP 2.0',
    'SolidWorks 2024',
    '' );
FILE_SCHEMA (( 'AUTOMOTIVE_DESIGN' ));
ENDSEC;

DATA;
#3=APPLICATION_CONTEXT ( 'automotive_design' ) ;
#7=DIRECTION ( 'NONE',  ( -0.000000000000000000, -1.000000000000000000, -0.000000000000000000 ) ) ;
#11=CARTESIAN_POINT ( 'NONE',  ( 0.000000000000000000, 0.000000000000000000, 0.000000000000000000 ) ) ;
#20=ORIENTED_EDGE ( 'NONE', *, *, #2616, .F. ) ;
#22=ORIENTED_EDGE ( 'NONE', *, *, #960, .T. ) ;
#40=EDGE_LOOP ( 'NONE', ( #5035, #3170, #2808, #3510 ) ) ;
#69=ORIENTED_EDGE ( 'NONE', *, *, #2616, .T. ) ;
#74=ORIENTED_EDGE ( 'NONE', *, *, #1802, .F. ) ;
#93=ORIENTED_EDGE ( 'NONE', *, *, #1802, .T. ) ;
#147=ORIENTED_EDGE ( 'NONE', *, *, #2271, .F. ) ;
#188=EDGE_LOOP ( 'NONE', ( #20, #5360, #4784, #93 ) ) ;
#191=CIRCLE ( 'NONE', #2391, 40.00000000000000000 ) ;
#201=CARTESIAN_POINT ( 'NONE',  ( 0.000000000000000000, 80.00000000000000000, 0.000000000000000000 ) ) ;
#282=UNCERTAINTY_MEASURE_WITH_UNIT (LENGTH_MEASURE( 1.000000000000000082E-05 ), #1628, 'distance_accuracy_value', 'NONE');
#314=CARTESIAN_POINT ( 'NONE',  ( 0.000000000000000000, 80.00000000000000000, -50.00000000000000000 ) ) ;
#395=AXIS2_PLACEMENT_3D ( 'NONE', #2077, #2901, #2570 ) ;
#408=CYLINDRICAL_SURFACE ( 'NONE', #1858, 50.00000000000000000 ) ;
#423=CYLINDRICAL_SURFACE ( 'NONE', #3820, 40.00000000000000000 ) ;
#427=CYLINDRICAL_SURFACE ( 'NONE', #395, 50.00000000000000000 ) ;
#441=ORIENTED_EDGE ( 'NONE', *, *, #3925, .T. ) ;
#449=ORIENTED_EDGE ( 'NONE', *, *, #5015, .T. ) ;
#482=CIRCLE ( 'NONE', #1008, 50.00000000000000000 ) ;
#543=LINE ( 'NONE', #1015, #833 ) ;
#550=ORIENTED_EDGE ( 'NONE', *, *, #5015, .F. ) ;
#557=VERTEX_POINT ( 'NONE', #3601 ) ;
#674=DIRECTION ( 'NONE',  ( 0.000000000000000000, 0.000000000000000000, 1.000000000000000000 ) ) ;
#692=ADVANCED_FACE ( 'NONE', ( #3776 ), #427, .T. ) ;
#719=FACE_BOUND ( 'NONE', #4120, .T. ) ;
#732=MECHANICAL_DESIGN_GEOMETRIC_PRESENTATION_REPRESENTATION('',(#2579),#4507);
#753=FACE_OUTER_BOUND ( 'NONE', #4113, .T. ) ;
#787=PRODUCT ( 'Conveyor Speed Sensor Mount', 'Conveyor Speed Sensor Mount', '', ( #3504 ) ) ;
#828=CARTESIAN_POINT ( 'NONE',  ( 0.000000000000000000, 80.00000000000000000, 0.000000000000000000 ) ) ;
#833=VECTOR ( 'NONE', #4801, 1000.000000000000000 ) ;
#844=DIRECTION ( 'NONE',  ( 0.000000000000000000, 0.000000000000000000, -1.000000000000000000 ) ) ;
#867=DIRECTION ( 'NONE',  ( 0.000000000000000000, 0.000000000000000000, 1.000000000000000000 ) ) ;
#877=( NAMED_UNIT ( * ) SI_UNIT ( $, .STERADIAN. ) SOLID_ANGLE_UNIT ( ) );
#896=AXIS2_PLACEMENT_3D ( 'NONE', #11, #3839, #867 ) ;
#898=EDGE_CURVE ( 'NONE', #5006, #1349, #5119, .T. ) ;
#928=PRODUCT_DEFINITION_FORMATION_WITH_SPECIFIED_SOURCE ( 'ANY', '', #787, .NOT_KNOWN. ) ;
#940=CARTESIAN_POINT ( 'NONE',  ( 6.123233995736766085E-15, 80.00000000000000000, 50.00000000000000000 ) ) ;
#959=DIRECTION ( 'NONE',  ( 0.000000000000000000, 0.000000000000000000, 1.000000000000000000 ) ) ;
#960=EDGE_CURVE ( 'NONE', #4918, #3848, #482, .T. ) ;
#977=CARTESIAN_POINT ( 'NONE',  ( 0.000000000000000000, 80.00000000000000000, 0.000000000000000000 ) ) ;
#978=( NAMED_UNIT ( * ) PLANE_ANGLE_UNIT ( ) SI_UNIT ( $, .RADIAN. ) );
#1005=CYLINDRICAL_SURFACE ( 'NONE', #3720, 40.00000000000000000 ) ;
#1008=AXIS2_PLACEMENT_3D ( 'NONE', #1026, #4765, #2630 ) ;
#1015=CARTESIAN_POINT ( 'NONE',  ( 0.000000000000000000, 80.00000000000000000, -50.00000000000000000 ) ) ;
#1026=CARTESIAN_POINT ( 'NONE',  ( 0.000000000000000000, 80.00000000000000000, 0.000000000000000000 ) ) ;
#1088=DIRECTION ( 'NONE',  ( 0.000000000000000000, 0.000000000000000000, 1.000000000000000000 ) ) ;
#1105=EDGE_LOOP ( 'NONE', ( #22, #441 ) ) ;
#1145=CARTESIAN_POINT ( 'NONE',  ( 0.000000000000000000, 0.000000000000000000, 0.000000000000000000 ) ) ;
#1151=VERTEX_POINT ( 'NONE', #4140 ) ;
#1226=FACE_OUTER_BOUND ( 'NONE', #188, .T. ) ;
#1246=ORIENTED_EDGE ( 'NONE', *, *, #1854, .F. ) ;
#1310=ORIENTED_EDGE ( 'NONE', *, *, #3718, .T. ) ;
#1347=DIRECTION ( 'NONE',  ( 1.000000000000000000, 0.000000000000000000, 0.000000000000000000 ) ) ;
#1349=VERTEX_POINT ( 'NONE', #3245 ) ;
#1388=CARTESIAN_POINT ( 'NONE',  ( 0.000000000000000000, 0.000000000000000000, 0.000000000000000000 ) ) ;
#1415=DIRECTION ( 'NONE',  ( 0.000000000000000000, 0.000000000000000000, -1.000000000000000000 ) ) ;
#1449=VERTEX_POINT ( 'NONE', #4485 ) ;
#1450=AXIS2_PLACEMENT_3D ( 'NONE', #2406, #4091, #2727 ) ;
#1512=ORIENTED_EDGE ( 'NONE', *, *, #4796, .F. ) ;
#1549=UNCERTAINTY_MEASURE_WITH_UNIT (LENGTH_MEASURE( 1.000000000000000082E-05 ), #1806, 'distance_accuracy_value', 'NONE');
#1595=AXIS2_PLACEMENT_3D ( 'NONE', #1145, #3602, #1088 ) ;
#1628=( LENGTH_UNIT ( ) NAMED_UNIT ( * ) SI_UNIT ( .MILLI., .METRE. ) );
#1657=DIRECTION ( 'NONE',  ( 0.000000000000000000, 1.000000000000000000, 0.000000000000000000 ) ) ;
#1667=DIRECTION ( 'NONE',  ( 0.000000000000000000, 1.000000000000000000, 0.000000000000000000 ) ) ;
#1680=CARTESIAN_POINT ( 'NONE',  ( 0.000000000000000000, 80.00000000000000000, 0.000000000000000000 ) ) ;
#1802=EDGE_CURVE ( 'NONE', #557, #1151, #2652, .T. ) ;
#1806=( LENGTH_UNIT ( ) NAMED_UNIT ( * ) SI_UNIT ( .MILLI., .METRE. ) );
#1853=EDGE_CURVE ( 'NONE', #5006, #1449, #191, .T. ) ;
#1854=EDGE_CURVE ( 'NONE', #4228, #1349, #4156, .T. ) ;
#1858=AXIS2_PLACEMENT_3D ( 'NONE', #1680, #4609, #844 ) ;
#1897=EDGE_LOOP ( 'NONE', ( #2430, #69, #5075, #5204 ) ) ;
#1942=ADVANCED_FACE ( 'NONE', ( #1226 ), #408, .T. ) ;
#1988=DIRECTION ( 'NONE',  ( 0.000000000000000000, 1.000000000000000000, 0.000000000000000000 ) ) ;
#2077=CARTESIAN_POINT ( 'NONE',  ( 0.000000000000000000, 80.00000000000000000, 0.000000000000000000 ) ) ;
#2110=ADVANCED_FACE ( 'NONE', ( #3129, #4794 ), #3969, .T. ) ;
#2166=DIRECTION ( 'NONE',  ( 0.000000000000000000, 0.000000000000000000, 1.000000000000000000 ) ) ;
#2227=( GEOMETRIC_REPRESENTATION_CONTEXT ( 3 ) GLOBAL_UNCERTAINTY_ASSIGNED_CONTEXT ( ( #282 ) ) GLOBAL_UNIT_ASSIGNED_CONTEXT ( ( #1628, #3850, #877 ) ) REPRESENTATION_CONTEXT ( 'NONE', 'WORKASPACE' ) );
#2236=CIRCLE ( 'NONE', #3557, 40.00000000000000000 ) ;
#2271=EDGE_CURVE ( 'NONE', #1449, #4228, #3267, .T. ) ;
#2273=DIRECTION ( 'NONE',  ( 0.000000000000000000, 1.000000000000000000, 0.000000000000000000 ) ) ;
#2305=ORIENTED_EDGE ( 'NONE', *, *, #898, .T. ) ;
#2322=PRODUCT_DEFINITION ( 'UNKNOWN', '', #928, #4515 ) ;
#2328=DIRECTION ( 'NONE',  ( 0.000000000000000000, 0.000000000000000000, 1.000000000000000000 ) ) ;
#2391=AXIS2_PLACEMENT_3D ( 'NONE', #2929, #1657, #2166 ) ;
#2406=CARTESIAN_POINT ( 'NONE',  ( 0.000000000000000000, 0.000000000000000000, 0.000000000000000000 ) ) ;
#2430=ORIENTED_EDGE ( 'NONE', *, *, #3925, .F. ) ;
#2445=CARTESIAN_POINT ( 'NONE',  ( 6.123233995736766085E-15, 80.00000000000000000, 50.00000000000000000 ) ) ;
#2570=DIRECTION ( 'NONE',  ( 0.000000000000000000, 0.000000000000000000, -1.000000000000000000 ) ) ;
#2579=STYLED_ITEM('',(#5479),#3126);
#2616=EDGE_CURVE ( 'NONE', #3848, #1151, #3039, .T. ) ;
#2623=DIRECTION ( 'NONE',  ( -0.000000000000000000, -1.000000000000000000, -0.000000000000000000 ) ) ;
#2628=ORIENTED_EDGE ( 'NONE', *, *, #1854, .T. ) ;
#2630=DIRECTION ( 'NONE',  ( 0.000000000000000000, 0.000000000000000000, 1.000000000000000000 ) ) ;
#2652=CIRCLE ( 'NONE', #1595, 50.00000000000000000 ) ;
#2671=CIRCLE ( 'NONE', #4082, 40.00000000000000000 ) ;
#2726=DIRECTION ( 'NONE',  ( 0.000000000000000000, 1.000000000000000000, 0.000000000000000000 ) ) ;
#2727=DIRECTION ( 'NONE',  ( 0.000000000000000000, -0.000000000000000000, 1.000000000000000000 ) ) ;
#2808=ORIENTED_EDGE ( 'NONE', *, *, #3718, .F. ) ;
#2827=SHAPE_DEFINITION_REPRESENTATION ( #4520, #3052 ) ;
#2892=DIRECTION ( 'NONE',  ( 0.000000000000000000, 0.000000000000000000, 1.000000000000000000 ) ) ;
#2898=DIRECTION ( 'NONE',  ( 0.000000000000000000, 0.000000000000000000, -1.000000000000000000 ) ) ;
#2901=DIRECTION ( 'NONE',  ( -0.000000000000000000, -1.000000000000000000, -0.000000000000000000 ) ) ;
#2926=AXIS2_PLACEMENT_3D ( 'NONE', #4646, #959, #1347 ) ;
#2929=CARTESIAN_POINT ( 'NONE',  ( 0.000000000000000000, 80.00000000000000000, 0.000000000000000000 ) ) ;
#3035=AXIS2_PLACEMENT_3D ( 'NONE', #5349, #4446, #674 ) ;
#3039=LINE ( 'NONE', #940, #3201 ) ;
#3052=SHAPE_REPRESENTATION ( 'Conveyor Speed Sensor Mount', ( #2926 ), #2227 ) ;
#3074=( NAMED_UNIT ( * ) SI_UNIT ( $, .STERADIAN. ) SOLID_ANGLE_UNIT ( ) );
#3098=CARTESIAN_POINT ( 'NONE',  ( 4.898587196589413815E-15, 0.000000000000000000, 40.00000000000000000 ) ) ;
#3126=MANIFOLD_SOLID_BREP ( 'Boss-Extrude1', #3332 ) ;
#3129=FACE_OUTER_BOUND ( 'NONE', #1105, .T. ) ;
#3170=ORIENTED_EDGE ( 'NONE', *, *, #2271, .T. ) ;
#3181=DIRECTION ( 'NONE',  ( 0.000000000000000000, -0.000000000000000000, 1.000000000000000000 ) ) ;
#3201=VECTOR ( 'NONE', #2623, 1000.000000000000000 ) ;
#3245=CARTESIAN_POINT ( 'NONE',  ( 0.000000000000000000, 0.000000000000000000, -40.00000000000000000 ) ) ;
#3267=LINE ( 'NONE', #4090, #5104 ) ;
#3332=CLOSED_SHELL ( 'NONE', ( #4196, #692, #2110, #4459, #1942, #4552 ) ) ;
#3384=VECTOR ( 'NONE', #3491, 1000.000000000000000 ) ;
#3433=ORIENTED_EDGE ( 'NONE', *, *, #1853, .F. ) ;
#3454=ADVANCED_BREP_SHAPE_REPRESENTATION ( '', ( #3126, #2926 ), #2227 ) ;
#3491=DIRECTION ( 'NONE',  ( -0.000000000000000000, -1.000000000000000000, -0.000000000000000000 ) ) ;
#3504=PRODUCT_CONTEXT ( 'NONE', #3, 'mechanical' ) ;
#3510=ORIENTED_EDGE ( 'NONE', *, *, #898, .F. ) ;
#3557=AXIS2_PLACEMENT_3D ( 'NONE', #4391, #2273, #2328 ) ;
#3601=CARTESIAN_POINT ( 'NONE',  ( 0.000000000000000000, 0.000000000000000000, -50.00000000000000000 ) ) ;
#3602=DIRECTION ( 'NONE',  ( 0.000000000000000000, 1.000000000000000000, 0.000000000000000000 ) ) ;
#3718=EDGE_CURVE ( 'NONE', #1349, #4228, #2236, .T. ) ;
#3720=AXIS2_PLACEMENT_3D ( 'NONE', #977, #5174, #1415 ) ;
#3776=FACE_OUTER_BOUND ( 'NONE', #1897, .T. ) ;
#3783=EDGE_CURVE ( 'NONE', #4918, #557, #543, .T. ) ;
#3820=AXIS2_PLACEMENT_3D ( 'NONE', #4142, #7, #2898 ) ;
#3839=DIRECTION ( 'NONE',  ( 0.000000000000000000, 1.000000000000000000, 0.000000000000000000 ) ) ;
#3848=VERTEX_POINT ( 'NONE', #2445 ) ;
#3850=( NAMED_UNIT ( * ) PLANE_ANGLE_UNIT ( ) SI_UNIT ( $, .RADIAN. ) );
#3925=EDGE_CURVE ( 'NONE', #3848, #4918, #4516, .T. ) ;
#3969=PLANE ( 'NONE',  #5374 ) ;
#4082=AXIS2_PLACEMENT_3D ( 'NONE', #828, #1667, #2892 ) ;
#4090=CARTESIAN_POINT ( 'NONE',  ( 4.898587196589413026E-15, 80.00000000000000000, 40.00000000000000000 ) ) ;
#4091=DIRECTION ( 'NONE',  ( 0.000000000000000000, 1.000000000000000000, 0.000000000000000000 ) ) ;
#4113=EDGE_LOOP ( 'NONE', ( #74, #1512 ) ) ;
#4120=EDGE_LOOP ( 'NONE', ( #1310, #2628 ) ) ;
#4136=CARTESIAN_POINT ( 'NONE',  ( 0.000000000000000000, 80.00000000000000000, -40.00000000000000000 ) ) ;
#4140=CARTESIAN_POINT ( 'NONE',  ( 6.123233995736766085E-15, 0.000000000000000000, 50.00000000000000000 ) ) ;
#4142=CARTESIAN_POINT ( 'NONE',  ( 0.000000000000000000, 80.00000000000000000, 0.000000000000000000 ) ) ;
#4156=CIRCLE ( 'NONE', #896, 40.00000000000000000 ) ;
#4170=FACE_OUTER_BOUND ( 'NONE', #4674, .T. ) ;
#4196=ADVANCED_FACE ( 'NONE', ( #4816 ), #1005, .F. ) ;
#4228=VERTEX_POINT ( 'NONE', #3098 ) ;
#4359=CARTESIAN_POINT ( 'NONE',  ( 0.000000000000000000, 80.00000000000000000, -40.00000000000000000 ) ) ;
#4391=CARTESIAN_POINT ( 'NONE',  ( 0.000000000000000000, 0.000000000000000000, 0.000000000000000000 ) ) ;
#4397=APPLICATION_CONTEXT ( 'automotive_design' ) ;
#4408=DIRECTION ( 'NONE',  ( -0.000000000000000000, -1.000000000000000000, -0.000000000000000000 ) ) ;
#4425=CIRCLE ( 'NONE', #4771, 50.00000000000000000 ) ;
#4446=DIRECTION ( 'NONE',  ( 0.000000000000000000, 1.000000000000000000, 0.000000000000000000 ) ) ;
#4459=ADVANCED_FACE ( 'NONE', ( #753, #719 ), #4840, .F. ) ;
#4485=CARTESIAN_POINT ( 'NONE',  ( 4.898587196589413815E-15, 80.00000000000000000, 40.00000000000000000 ) ) ;
#4507=( GEOMETRIC_REPRESENTATION_CONTEXT ( 3 ) GLOBAL_UNCERTAINTY_ASSIGNED_CONTEXT ( ( #1549 ) ) GLOBAL_UNIT_ASSIGNED_CONTEXT ( ( #1806, #978, #3074 ) ) REPRESENTATION_CONTEXT ( 'NONE', 'WORKASPACE' ) );
#4515=PRODUCT_DEFINITION_CONTEXT ( 'detailed design', #4397, 'design' ) ;
#4516=CIRCLE ( 'NONE', #3035, 50.00000000000000000 ) ;
#4520=PRODUCT_DEFINITION_SHAPE ( 'NONE', 'NONE',  #2322 ) ;
#4552=ADVANCED_FACE ( 'NONE', ( #4170 ), #423, .F. ) ;
#4609=DIRECTION ( 'NONE',  ( -0.000000000000000000, -1.000000000000000000, -0.000000000000000000 ) ) ;
#4646=CARTESIAN_POINT ( 'NONE',  ( 0.000000000000000000, 0.000000000000000000, 0.000000000000000000 ) ) ;
#4674=EDGE_LOOP ( 'NONE', ( #147, #449, #2305, #1246 ) ) ;
#4764=EDGE_LOOP ( 'NONE', ( #3433, #550 ) ) ;
#4765=DIRECTION ( 'NONE',  ( 0.000000000000000000, 1.000000000000000000, 0.000000000000000000 ) ) ;
#4771=AXIS2_PLACEMENT_3D ( 'NONE', #1388, #1988, #5334 ) ;
#4784=ORIENTED_EDGE ( 'NONE', *, *, #3783, .T. ) ;
#4794=FACE_BOUND ( 'NONE', #4764, .T. ) ;
#4796=EDGE_CURVE ( 'NONE', #1151, #557, #4425, .T. ) ;
#4801=DIRECTION ( 'NONE',  ( -0.000000000000000000, -1.000000000000000000, -0.000000000000000000 ) ) ;
#4816=FACE_OUTER_BOUND ( 'NONE', #40, .T. ) ;
#4840=PLANE ( 'NONE',  #1450 ) ;
#4918=VERTEX_POINT ( 'NONE', #314 ) ;
#5006=VERTEX_POINT ( 'NONE', #4136 ) ;
#5015=EDGE_CURVE ( 'NONE', #1449, #5006, #2671, .T. ) ;
#5035=ORIENTED_EDGE ( 'NONE', *, *, #1853, .T. ) ;
#5075=ORIENTED_EDGE ( 'NONE', *, *, #4796, .T. ) ;
#5104=VECTOR ( 'NONE', #4408, 1000.000000000000000 ) ;
#5119=LINE ( 'NONE', #4359, #3384 ) ;
#5174=DIRECTION ( 'NONE',  ( -0.000000000000000000, -1.000000000000000000, -0.000000000000000000 ) ) ;
#5204=ORIENTED_EDGE ( 'NONE', *, *, #3783, .F. ) ;
#5334=DIRECTION ( 'NONE',  ( 0.000000000000000000, 0.000000000000000000, 1.000000000000000000 ) ) ;
#5349=CARTESIAN_POINT ( 'NONE',  ( 0.000000000000000000, 80.00000000000000000, 0.000000000000000000 ) ) ;
#5360=ORIENTED_EDGE ( 'NONE', *, *, #960, .F. ) ;
#5374=AXIS2_PLACEMENT_3D ( 'NONE', #201, #2726, #3181 ) ;
#5432=SHAPE_REPRESENTATION_RELATIONSHIP ( 'NONE' , 'NONE' ,  #3052, #3454 ) ;
#5473=COLOUR_RGB('Off White',0.89,0.88,0.83);
#5474=FILL_AREA_STYLE_COLOUR('',#5473);
#5475=FILL_AREA_STYLE('',(#5474));
#5476=SURFACE_STYLE_FILL_AREA(#5475);
#5477=SURFACE_SIDE_STYLE('',(#5476));
#5478=SURFACE_STYLE_USAGE(.BOTH.,#5477);
#5479=PRESENTATION_STYLE_ASSIGNMENT((#5478));
ENDSEC;
END-ISO-10303-21;
